ISO-10303-21;
HEADER;
FILE_DESCRIPTION (('STEP AP214'),
    '1' );
FILE_NAME ('9. Reciprocating Link.step',
    '2026-10-09T14:04:53',
    ( '' ),
    ( '' ),
    'SwSTEP 2.0',
    'SolidWorks 2021',
    '' );
FILE_SCHEMA (( 'AUTOMOTIVE_DESIGN' ));
ENDSEC;

DATA;
#143=CARTESIAN_POINT ( 'NONE',  ( 0.5376128474930174095, 13.88012476438581544, 6.984229002090723171 ) ) ;
#178=CARTESIAN_POINT ( 'NONE',  ( 2.022166183945757645, 14.39193082815908831, -6.705330260831378730 ) ) ;
#190=ORIENTED_EDGE ( 'NONE', *, *, #68395, .T. ) ;
#342=EDGE_CURVE ( 'NONE', #9727, #28736, #74562, .T. ) ;
#438=CARTESIAN_POINT ( 'NONE',  ( 0.2708782075111812460, 21.85270131633358304, -7.000000000000008882 ) ) ;
#531=AXIS2_PLACEMENT_3D ( 'NONE', #35055, #67923, #93265 ) ;
#581=CARTESIAN_POINT ( 'NONE',  ( -2.026673642932869779, 21.31079249973476308, -6.703948387959501432 ) ) ;
#663=CARTESIAN_POINT ( 'NONE',  ( 2.025576785233600852, 14.39373949114980178, 6.704368252951605989 ) ) ;
#742=ORIENTED_EDGE ( 'NONE', *, *, #53663, .T. ) ;
#1096=CARTESIAN_POINT ( 'NONE',  ( -3.172455242975765533, 15.40272630234914253, 6.241991285340878548 ) ) ;
#1313=AXIS2_PLACEMENT_3D ( 'NONE', #34707, #83734, #100461 ) ;
#1646=CARTESIAN_POINT ( 'NONE',  ( -2.649051870092321792, 14.84475683689757908, 6.482396460464982191 ) ) ;
#1793=CARTESIAN_POINT ( 'NONE',  ( 3.585532980576127571, 16.06055535235176635, -6.013159465609652088 ) ) ;
#2279=PLANE ( 'NONE',  #1313 ) ;
#3003=( LENGTH_UNIT ( ) NAMED_UNIT ( * ) SI_UNIT ( .MILLI., .METRE. ) );
#3441=ORIENTED_EDGE ( 'NONE', *, *, #47097, .F. ) ;
#3533=AXIS2_PLACEMENT_3D ( 'NONE', #82497, #91140, #8598 ) ;
#3691=CARTESIAN_POINT ( 'NONE',  ( -3.860250758805052307, 18.90906293816489026, 5.839574874194349619 ) ) ;
#3693=PRODUCT_DEFINITION_SHAPE ( 'NONE', 'NONE',  #43009 ) ;
#3846=PRESENTATION_STYLE_ASSIGNMENT (( #62614 ) ) ;
#3970=CARTESIAN_POINT ( 'NONE',  ( 0.000000000000000000, 2.999999999999993339, 0.000000000000000000 ) ) ;
#4213=CARTESIAN_POINT ( 'NONE',  ( -3.177887466246608117, 20.29553532598250598, 6.239201926316404467 ) ) ;
#4575=ORIENTED_EDGE ( 'NONE', *, *, #72345, .F. ) ;
#4747=FACE_BOUND ( 'NONE', #34920, .T. ) ;
#4905=FILL_AREA_STYLE ('',( #104109 ) ) ;
#5098=CIRCLE ( 'NONE', #63620, 7.000000000000011546 ) ;
#5412=ADVANCED_FACE ( 'NONE', ( #65351 ), #81500, .T. ) ;
#5432=FACE_OUTER_BOUND ( 'NONE', #12491, .T. ) ;
#5544=ORIENTED_EDGE ( 'NONE', *, *, #78358, .T. ) ;
#5737=COLOUR_RGB ( '', 0.40784314, 0.44705882, 0.49803922) ;
#6128=DIRECTION ( 'NONE',  ( -0.000000000000000000, -1.000000000000000000, -0.000000000000000000 ) ) ;
#6234=EDGE_LOOP ( 'NONE', ( #47230, #47936, #742, #19639, #46419, #100395 ) ) ;
#6376=FACE_OUTER_BOUND ( 'NONE', #56628, .T. ) ;
#6848=PRODUCT_DEFINITION_CONTEXT ( 'detailed design', #28730, 'design' ) ;
#7377=CARTESIAN_POINT ( 'NONE',  ( -3.222962768498216414E-17, 13.85270131633358304, -7.000000000000011546 ) ) ;
#7421=CARTESIAN_POINT ( 'NONE',  ( 0.000000000000000000, 0.000000000000000000, -7.000000000000011546 ) ) ;
#7472=VECTOR ( 'NONE', #55440, 1000.000000000000000 ) ;
#7710=SHAPE_DEFINITION_REPRESENTATION ( #3693, #58557 ) ;
#7720=EDGE_CURVE ( 'NONE', #28736, #29611, #72331, .T. ) ;
#7958=CARTESIAN_POINT ( 'NONE',  ( 0.000000000000000000, 200.0000000000000000, 2.000000000000011102 ) ) ;
#8264=DIRECTION ( 'NONE',  ( 0.000000000000000000, 1.000000000000000000, 0.000000000000000000 ) ) ;
#8275=ORIENTED_EDGE ( 'NONE', *, *, #68395, .F. ) ;
#8302=CARTESIAN_POINT ( 'NONE',  ( 3.972805511173104875, 17.31670332531925283, -5.763756076061313571 ) ) ;
#8317=CARTESIAN_POINT ( 'NONE',  ( 0.000000000000000000, 2.999999999999992895, -7.000000000000024869 ) ) ;
#8598=DIRECTION ( 'NONE',  ( 0.000000000000000000, 0.000000000000000000, 1.000000000000000000 ) ) ;
#9313=CARTESIAN_POINT ( 'NONE',  ( 3.972742726731588458, 17.31622427227530636, 5.763799860841350764 ) ) ;
#9364=PLANE ( 'NONE',  #42669 ) ;
#9727=VERTEX_POINT ( 'NONE', #40312 ) ;
#9766=CARTESIAN_POINT ( 'NONE',  ( -1.800054524762938479, 21.43447476329978585, -6.769169511956039997 ) ) ;
#10113=CARTESIAN_POINT ( 'NONE',  ( 1.224646799147353454E-15, -6.505213034913025026E-15, 10.00000000000000178 ) ) ;
#10127=EDGE_LOOP ( 'NONE', ( #22857, #190, #38734, #60532, #97023, #67420, #58974, #68190, #91879, #15491 ) ) ;
#10147=EDGE_CURVE ( 'NONE', #89487, #9727, #77997, .T. ) ;
#10206=CYLINDRICAL_SURFACE ( 'NONE', #531, 10.00000000000000178 ) ;
#10281=CARTESIAN_POINT ( 'NONE',  ( -3.972557191600006643, 17.31504860060557505, 5.763927351470794491 ) ) ;
#10450=FACE_OUTER_BOUND ( 'NONE', #79671, .T. ) ;
#10554=PRESENTATION_STYLE_ASSIGNMENT (( #35954 ) ) ;
#10728=AXIS2_PLACEMENT_3D ( 'NONE', #14983, #57033, #47878 ) ;
#10739=VECTOR ( 'NONE', #87692, 1000.000000000000000 ) ;
#11119=DIRECTION ( 'NONE',  ( 1.000000000000000000, 0.000000000000000000, 0.000000000000000000 ) ) ;
#11614=( NAMED_UNIT ( * ) PLANE_ANGLE_UNIT ( ) SI_UNIT ( $, .RADIAN. ) );
#11941=VERTEX_POINT ( 'NONE', #29986 ) ;
#12003=EDGE_CURVE ( 'NONE', #82223, #17102, #70755, .T. ) ;
#12361=AXIS2_PLACEMENT_3D ( 'NONE', #42900, #44506, #91976 ) ;
#12491=EDGE_LOOP ( 'NONE', ( #90565, #61291, #51792, #105300 ) ) ;
#13501=DIRECTION ( 'NONE',  ( 0.000000000000000000, 1.000000000000000000, 0.000000000000000000 ) ) ;
#13624=AXIS2_PLACEMENT_3D ( 'NONE', #3970, #46025, #103718 ) ;
#13658=AXIS2_PLACEMENT_3D ( 'NONE', #103822, #88183, #79022 ) ;
#13758=DIRECTION ( 'NONE',  ( -1.000000000000000000, 0.000000000000000000, 0.000000000000000000 ) ) ;
#14000=CARTESIAN_POINT ( 'NONE',  ( 4.000000000000000000, 17.85270131633358304, 5.744562646538042827 ) ) ;
#14213=VERTEX_POINT ( 'NONE', #67027 ) ;
#14216=CARTESIAN_POINT ( 'NONE',  ( -0.5360553870754001249, 13.87989746200968710, -6.984358482147105640 ) ) ;
#14264=DIRECTION ( 'NONE',  ( -0.000000000000000000, -1.000000000000000000, -0.000000000000000000 ) ) ;
#14518=B_SPLINE_CURVE_WITH_KNOTS ( 'NONE', 3,
 ( #18010, #50876, #8302, #81639, #57906, #1793, #58459, #74093, #34214, #67086, #50344, #178, #66011, #67622, #98889, #59537, #42259, #48745, #75150, #83779 ),
 .UNSPECIFIED., .F., .F.,
 ( 4, 2, 2, 2, 2, 2, 2, 2, 2, 4 ),
 ( 0.006400020579250047421, 0.007199736318437515055, 0.007999452057624981821, 0.008799167796812449455, 0.009598883535999917088, 0.01039859927518738472, 0.01119831501437485236, 0.01159817288396858617, 0.01199803075356231825, 0.01279774649274978589 ),
 .UNSPECIFIED. ) ;
#14521=CARTESIAN_POINT ( 'NONE',  ( 1.313512443508423777, 21.63996318350142545, -6.880116371441049594 ) ) ;
#14645=VERTEX_POINT ( 'NONE', #59894 ) ;
#14728=( NAMED_UNIT ( * ) PLANE_ANGLE_UNIT ( ) SI_UNIT ( $, .RADIAN. ) );
#14983=CARTESIAN_POINT ( 'NONE',  ( 0.000000000000000000, 0.000000000000000000, 0.000000000000000000 ) ) ;
#15275=( NAMED_UNIT ( * ) SI_UNIT ( $, .STERADIAN. ) SOLID_ANGLE_UNIT ( ) );
#15301=CARTESIAN_POINT ( 'NONE',  ( 3.787353845334695546, 16.54002813235528535, 5.888118072323124785 ) ) ;
#15491=ORIENTED_EDGE ( 'NONE', *, *, #97547, .F. ) ;
#15731=CARTESIAN_POINT ( 'NONE',  ( 0.000000000000000000, 0.000000000000000000, 0.000000000000000000 ) ) ;
#15760=ORIENTED_EDGE ( 'NONE', *, *, #78358, .F. ) ;
#15904=ORIENTED_EDGE ( 'NONE', *, *, #32316, .F. ) ;
#16131=CARTESIAN_POINT ( 'NONE',  ( 4.000000000000000888, 18.12356304358896608, -5.744562646538073913 ) ) ;
#16133=ORIENTED_EDGE ( 'NONE', *, *, #12003, .T. ) ;
#16332=( NAMED_UNIT ( * ) PLANE_ANGLE_UNIT ( ) SI_UNIT ( $, .RADIAN. ) );
#16358=CARTESIAN_POINT ( 'NONE',  ( 3.866984248298421356, 16.79585448967792516, 5.835281178490491882 ) ) ;
#16427=B_SPLINE_CURVE_WITH_KNOTS ( 'NONE', 3,
 ( #31438, #72903, #98775, #49704, #105813, #49157, #82063, #96673, #55645, #82609, #18432, #581, #9766, #100380, #66969, #26543, #91773, #50236 ),
 .UNSPECIFIED., .F., .F.,
 ( 4, 2, 2, 2, 2, 2, 2, 2, 4 ),
 ( 0.01918577306495539495, 0.01998357421775985229, 0.02078137537056430964, 0.02157917652336876352, 0.02237697767617322087, 0.02317477882897767821, 0.02397257998178213556, 0.02477038113458659291, 0.02556818228739105026 ),
 .UNSPECIFIED. ) ;
#16910=FACE_OUTER_BOUND ( 'NONE', #33756, .T. ) ;
#16952=CARTESIAN_POINT ( 'NONE',  ( 1.224646799147353454E-15, 0.000000000000000000, 10.00000000000000178 ) ) ;
#17013=EDGE_CURVE ( 'NONE', #21895, #36223, #23121, .T. ) ;
#17102=VERTEX_POINT ( 'NONE', #7958 ) ;
#17313=SURFACE_SIDE_STYLE ('',( #91206 ) ) ;
#17956=COLOUR_RGB ( '', 0.40784314, 0.44705882, 0.49803922) ;
#18010=CARTESIAN_POINT ( 'NONE',  ( 4.000000000000000000, 17.85270131633358304, -5.744562646538043715 ) ) ;
#18198=ADVANCED_FACE ( 'NONE', ( #6376 ), #105097, .T. ) ;
#18302=AXIS2_PLACEMENT_3D ( 'NONE', #66545, #99422, #26657 ) ;
#18399=CARTESIAN_POINT ( 'NONE',  ( 0.000000000000000000, 2.999999999999992450, -7.000000000000024869 ) ) ;
#18432=CARTESIAN_POINT ( 'NONE',  ( -2.451784423852116035, 21.02359296169644054, -6.560417912171430110 ) ) ;
#18690=SURFACE_STYLE_FILL_AREA ( #92010 ) ;
#18983=ADVANCED_FACE ( 'NONE', ( #5432 ), #60884, .T. ) ;
#18989=CARTESIAN_POINT ( 'NONE',  ( 3.972708858246882357, 18.38910731443329638, 5.763820867899048572 ) ) ;
#19357=CIRCLE ( 'NONE', #12361, 5.000000000000000000 ) ;
#19425=CARTESIAN_POINT ( 'NONE',  ( -4.000000000000000000, 17.85270131633358659, -5.744562646538044604 ) ) ;
#19581=( GEOMETRIC_REPRESENTATION_CONTEXT ( 3 ) GLOBAL_UNCERTAINTY_ASSIGNED_CONTEXT ( ( #81258 ) ) GLOBAL_UNIT_ASSIGNED_CONTEXT ( ( #96212, #14728, #15275 ) ) REPRESENTATION_CONTEXT ( 'NONE', 'WORKASPACE' ) );
#19639=ORIENTED_EDGE ( 'NONE', *, *, #72345, .T. ) ;
#19889=EDGE_CURVE ( 'NONE', #14645, #68407, #73563, .T. ) ;
#19910=CARTESIAN_POINT ( 'NONE',  ( -1.798493680560833141, 21.43522084520895277, 6.769567297170397957 ) ) ;
#19969=ORIENTED_EDGE ( 'NONE', *, *, #100235, .T. ) ;
#20369=B_SPLINE_CURVE_WITH_KNOTS ( 'NONE', 3,
 ( #46599, #21831, #14216, #39059, #54670, #88654, #103251, #21302, #70879, #80546, #62799, #47649, #29396, #55725, #103773, #94650, #79497, #95687 ),
 .UNSPECIFIED., .F., .F.,
 ( 4, 2, 2, 2, 2, 2, 2, 2, 4 ),
 ( 0.01279774649274978589, 0.01359624981427548680, 0.01439475313580118598, 0.01519325645732688690, 0.01599175977885258781, 0.01679026310037829567, 0.01758876642190399311, 0.01838726974342969403, 0.01918577306495539495 ),
 .UNSPECIFIED. ) ;
#21302=CARTESIAN_POINT ( 'NONE',  ( -2.455881507267896779, 14.68468481912377754, -6.558993639549812293 ) ) ;
#21643=( NAMED_UNIT ( * ) SI_UNIT ( $, .STERADIAN. ) SOLID_ANGLE_UNIT ( ) );
#21831=CARTESIAN_POINT ( 'NONE',  ( -0.2707382100857756990, 13.85270131633358837, -7.000000000000010658 ) ) ;
#21895=VERTEX_POINT ( 'NONE', #7377 ) ;
#22010=CARTESIAN_POINT ( 'NONE',  ( -3.014384158603856445, 20.49438651917788334, 6.320775516481683454 ) ) ;
#22114=ORIENTED_EDGE ( 'NONE', *, *, #43290, .F. ) ;
#22369=ORIENTED_EDGE ( 'NONE', *, *, #43312, .T. ) ;
#22408=CARTESIAN_POINT ( 'NONE',  ( 8.595526037062774425E-16, 13.85270131633358304, 7.000000000000011546 ) ) ;
#22515=EDGE_LOOP ( 'NONE', ( #39895, #28541 ) ) ;
#22857=ORIENTED_EDGE ( 'NONE', *, *, #33609, .T. ) ;
#22869=SURFACE_STYLE_USAGE ( .BOTH. , #97250 ) ;
#23121=LINE ( 'NONE', #7421, #7472 ) ;
#23198=APPLICATION_CONTEXT ( 'automotive_design' ) ;
#23265=DIRECTION ( 'NONE',  ( -0.000000000000000000, -1.000000000000000000, -0.000000000000000000 ) ) ;
#23939=( NAMED_UNIT ( * ) SI_UNIT ( $, .STERADIAN. ) SOLID_ANGLE_UNIT ( ) );
#23969=CARTESIAN_POINT ( 'NONE',  ( 1.797717371853386981, 14.26981950330974946, 6.769760908209460304 ) ) ;
#24243=ORIENTED_EDGE ( 'NONE', *, *, #101460, .T. ) ;
#24263=CIRCLE ( 'NONE', #3533, 2.000000000000011102 ) ;
#24279=DIRECTION ( 'NONE',  ( -0.000000000000000000, -1.000000000000000000, -0.000000000000000000 ) ) ;
#24473=PRESENTATION_STYLE_ASSIGNMENT (( #22869 ) ) ;
#24746=CARTESIAN_POINT ( 'NONE',  ( 0.2690448671709230188, 21.85270131633360435, 7.000000000000021316 ) ) ;
#25199=ADVANCED_FACE ( 'NONE', ( #16910 ), #32579, .T. ) ;
#25996=CARTESIAN_POINT ( 'NONE',  ( -3.787333677597864323, 16.53967541042004186, 5.888147140825949144 ) ) ;
#26020=ORIENTED_EDGE ( 'NONE', *, *, #17013, .T. ) ;
#26367=CARTESIAN_POINT ( 'NONE',  ( 1.793818517922412203, 21.43745688976599695, 6.770759481125232071 ) ) ;
#26543=CARTESIAN_POINT ( 'NONE',  ( -0.5402994271758849720, 21.82491192351207587, -6.984019969325498955 ) ) ;
#26657=DIRECTION ( 'NONE',  ( 0.000000000000000000, 0.000000000000000000, -1.000000000000000000 ) ) ;
#26676=AXIS2_PLACEMENT_3D ( 'NONE', #35128, #76076, #57753 ) ;
#27221=CYLINDRICAL_SURFACE ( 'NONE', #72388, 4.000000000000000000 ) ;
#27457=LINE ( 'NONE', #60857, #58258 ) ;
#27586=CARTESIAN_POINT ( 'NONE',  ( -1.053783150697139126, 13.98491295135151447, 6.925164142196040373 ) ) ;
#27886=EDGE_LOOP ( 'NONE', ( #22369, #37253 ) ) ;
#28541=ORIENTED_EDGE ( 'NONE', *, *, #72828, .F. ) ;
#28730=APPLICATION_CONTEXT ( 'automotive_design' ) ;
#28736=VERTEX_POINT ( 'NONE', #22408 ) ;
#29075=CARTESIAN_POINT ( 'NONE',  ( -2.654566931710991007, 20.85574759830042524, 6.480122636992501128 ) ) ;
#29263=DIRECTION ( 'NONE',  ( 0.000000000000000000, 0.000000000000000000, 1.000000000000000000 ) ) ;
#29396=CARTESIAN_POINT ( 'NONE',  ( -3.585543761590458178, 16.06066171126383324, -6.013148396082499403 ) ) ;
#29611=VERTEX_POINT ( 'NONE', #14000 ) ;
#29684=DIRECTION ( 'NONE',  ( 0.000000000000000000, 0.000000000000000000, -1.000000000000000000 ) ) ;
#29970=ADVANCED_FACE ( 'NONE', ( #4747, #103439 ), #9364, .T. ) ;
#29986=CARTESIAN_POINT ( 'NONE',  ( 4.010857135589731489E-16, 21.85270131633359014, 7.000000000000016875 ) ) ;
#30099=CARTESIAN_POINT ( 'NONE',  ( -3.782179052920016105, 19.16134848367324039, 5.890440751236702077 ) ) ;
#30423=FILL_AREA_STYLE_COLOUR ( '', #5737 ) ;
#31085=DIRECTION ( 'NONE',  ( 0.000000000000000000, 1.000000000000000000, 0.000000000000000000 ) ) ;
#31236=DIRECTION ( 'NONE',  ( 0.000000000000000000, 0.000000000000000000, -1.000000000000000000 ) ) ;
#31438=CARTESIAN_POINT ( 'NONE',  ( -4.000000000000000000, 17.85270131633358659, -5.744562646538044604 ) ) ;
#31486=VERTEX_POINT ( 'NONE', #101952 ) ;
#32081=CIRCLE ( 'NONE', #18302, 7.000000000000024869 ) ;
#32316=EDGE_CURVE ( 'NONE', #89487, #50732, #16427, .T. ) ;
#32578=CARTESIAN_POINT ( 'NONE',  ( 8.595526037062774425E-16, 13.85270131633358304, 7.000000000000011546 ) ) ;
#32579=PLANE ( 'NONE',  #42632 ) ;
#32880=CARTESIAN_POINT ( 'NONE',  ( 1.056274524463007403, 21.71983277640987353, -6.924796165863814856 ) ) ;
#32994=EDGE_CURVE ( 'NONE', #70408, #14645, #48032, .T. ) ;
#33305=ORIENTED_EDGE ( 'NONE', *, *, #32994, .T. ) ;
#33329=STYLED_ITEM ( 'NONE', ( #3846 ), #18983 ) ;
#33409=CARTESIAN_POINT ( 'NONE',  ( 2.024297636968084735, 21.31243181164073874, -6.704763639156325006 ) ) ;
#33583=LINE ( 'NONE', #72943, #41583 ) ;
#33609=EDGE_CURVE ( 'NONE', #105779, #82223, #5098, .T. ) ;
#33629=CARTESIAN_POINT ( 'NONE',  ( 3.013809335369860509, 15.21035869299223009, 6.321051127802831182 ) ) ;
#33756=EDGE_LOOP ( 'NONE', ( #24243, #64907 ) ) ;
#34071=CARTESIAN_POINT ( 'NONE',  ( -3.010034769234505525, 15.20602481743756051, 6.322865676976533678 ) ) ;
#34138=DIRECTION ( 'NONE',  ( -0.000000000000000000, -1.000000000000000000, -0.000000000000000000 ) ) ;
#34214=CARTESIAN_POINT ( 'NONE',  ( 3.011045263346121992, 15.20713166912945624, -6.322393913128321330 ) ) ;
#34607=CARTESIAN_POINT ( 'NONE',  ( -2.020600889975352921, 14.39097068952101743, 6.705821464114419150 ) ) ;
#34707=CARTESIAN_POINT ( 'NONE',  ( 0.000000000000000000, -3.252606517456512513E-15, -10.00000000000000178 ) ) ;
#34875=SURFACE_SIDE_STYLE ('',( #18690 ) ) ;
#34920=EDGE_LOOP ( 'NONE', ( #65377, #78131 ) ) ;
#35055=CARTESIAN_POINT ( 'NONE',  ( 0.000000000000000000, 0.000000000000000000, 0.000000000000000000 ) ) ;
#35128=CARTESIAN_POINT ( 'NONE',  ( 0.000000000000000000, 2.999999999999992450, 0.000000000000000000 ) ) ;
#35295=DIRECTION ( 'NONE',  ( -0.000000000000000000, -0.000000000000000000, 1.000000000000000000 ) ) ;
#35300=DIRECTION ( 'NONE',  ( -0.000000000000000000, -0.000000000000000000, 1.000000000000000000 ) ) ;
#35954=SURFACE_STYLE_USAGE ( .BOTH. , #34875 ) ;
#36223=VERTEX_POINT ( 'NONE', #18399 ) ;
#36240=CARTESIAN_POINT ( 'NONE',  ( 3.867302399549911840, 18.90821977549292043, 5.835068021887773071 ) ) ;
#36741=CARTESIAN_POINT ( 'NONE',  ( -0.2696830121834116190, 13.85270131633358304, 7.000000000000015987 ) ) ;
#37253=ORIENTED_EDGE ( 'NONE', *, *, #47097, .T. ) ;
#37684=CARTESIAN_POINT ( 'NONE',  ( -3.465069528698219603, 19.86757101636677447, 6.084398292909884987 ) ) ;
#38029=AXIS2_PLACEMENT_3D ( 'NONE', #67543, #34138, #99892 ) ;
#38734=ORIENTED_EDGE ( 'NONE', *, *, #85769, .F. ) ;
#39052=PRODUCT_CONTEXT ( 'NONE', #23198, 'mechanical' ) ;
#39059=CARTESIAN_POINT ( 'NONE',  ( -1.056558204502631382, 13.98563387401484981, -6.924760179648891345 ) ) ;
#39895=ORIENTED_EDGE ( 'NONE', *, *, #32994, .F. ) ;
#40312=CARTESIAN_POINT ( 'NONE',  ( -4.000000000000000000, 17.85270131633358304, 5.744562646538042827 ) ) ;
#40538=DIRECTION ( 'NONE',  ( -0.000000000000000000, -1.000000000000000000, -0.000000000000000000 ) ) ;
#41176=CARTESIAN_POINT ( 'NONE',  ( 1.057586783462449942, 13.98593235112240940, 6.924593311009700436 ) ) ;
#41177=DIRECTION ( 'NONE',  ( 0.000000000000000000, -0.000000000000000000, 1.000000000000000000 ) ) ;
#41473=CARTESIAN_POINT ( 'NONE',  ( 4.000000000000000000, 17.85270131633358304, -5.744562646538043715 ) ) ;
#41583=VECTOR ( 'NONE', #57822, 1000.000000000000000 ) ;
#41962=CARTESIAN_POINT ( 'NONE',  ( 1.312288883421210306, 21.64033319957477985, 6.880324608108087325 ) ) ;
#42148=CIRCLE ( 'NONE', #38029, 10.00000000000000178 ) ;
#42223=CARTESIAN_POINT ( 'NONE',  ( 0.2692838627284316333, 13.85270131633357593, 7.000000000000015099 ) ) ;
#42259=CARTESIAN_POINT ( 'NONE',  ( 0.9250510724394636064, 13.95888890799997384, -6.939834513072449695 ) ) ;
#42477=CARTESIAN_POINT ( 'NONE',  ( 8.572527594031486009E-16, 0.000000000000000000, 7.000000000000011546 ) ) ;
#42531=CARTESIAN_POINT ( 'NONE',  ( -0.1342739691912682998, 21.85270131633359725, 7.000000000000020428 ) ) ;
#42598=CIRCLE ( 'NONE', #58071, 2.000000000000011102 ) ;
#42632=AXIS2_PLACEMENT_3D ( 'NONE', #65454, #8264, #41177 ) ;
#42653=CARTESIAN_POINT ( 'NONE',  ( -3.461462603046343123, 15.83153173276467385, 6.086477152069783791 ) ) ;
#42669=AXIS2_PLACEMENT_3D ( 'NONE', #8317, #99442, #57926 ) ;
#42900=CARTESIAN_POINT ( 'NONE',  ( 2.449293598294720219E-16, 195.0000000000000000, -2.000000000000011102 ) ) ;
#43009=PRODUCT_DEFINITION ( 'UNKNOWN', '', #59420, #6848 ) ;
#43053=ORIENTED_EDGE ( 'NONE', *, *, #43290, .T. ) ;
#43193=CARTESIAN_POINT ( 'NONE',  ( -2.448089827929017304, 14.67886088499936292, 6.561838588348337886 ) ) ;
#43227=CARTESIAN_POINT ( 'NONE',  ( 3.191145750007355009, 20.31792217114059795, 6.242773338886944856 ) ) ;
#43290=EDGE_CURVE ( 'NONE', #21895, #89487, #20369, .T. ) ;
#43312=EDGE_CURVE ( 'NONE', #98268, #68407, #96272, .T. ) ;
#43364=CARTESIAN_POINT ( 'NONE',  ( 0.000000000000000000, 17.85270131633358304, -10.00000000000000178 ) ) ;
#43386=VECTOR ( 'NONE', #75702, 1000.000000000000000 ) ;
#43602=CARTESIAN_POINT ( 'NONE',  ( -0.2701126386571010007, 21.84581818726675095, 6.996060251427160814 ) ) ;
#43689=( GEOMETRIC_REPRESENTATION_CONTEXT ( 3 ) GLOBAL_UNCERTAINTY_ASSIGNED_CONTEXT ( ( #90450 ) ) GLOBAL_UNIT_ASSIGNED_CONTEXT ( ( #54479, #95500, #21643 ) ) REPRESENTATION_CONTEXT ( 'NONE', 'WORKASPACE' ) );
#43805=MECHANICAL_DESIGN_GEOMETRIC_PRESENTATION_REPRESENTATION('',(#90312),#55791);
#44506=DIRECTION ( 'NONE',  ( 1.000000000000000000, -0.000000000000000000, 1.224646799147353207E-16 ) ) ;
#44686=CARTESIAN_POINT ( 'NONE',  ( -1.314451062625864530, 21.63968482537510241, 6.879959252342844778 ) ) ;
#45332=CARTESIAN_POINT ( 'NONE',  ( -0.5342533769375044095, 13.87968997803932503, 6.984477836909634085 ) ) ;
#45370=DIRECTION ( 'NONE',  ( 0.000000000000000000, 0.000000000000000000, 1.000000000000000000 ) ) ;
#46025=DIRECTION ( 'NONE',  ( -0.000000000000000000, -1.000000000000000000, -0.000000000000000000 ) ) ;
#46268=CARTESIAN_POINT ( 'NONE',  ( -2.026245759303455518, 21.31123701474006182, 6.704152251160012455 ) ) ;
#46419=ORIENTED_EDGE ( 'NONE', *, *, #85769, .T. ) ;
#46599=CARTESIAN_POINT ( 'NONE',  ( -3.222962768498216414E-17, 13.85270131633358304, -7.000000000000011546 ) ) ;
#46653=AXIS2_PLACEMENT_3D ( 'NONE', #98130, #24279, #99180 ) ;
#46668=DIRECTION ( 'NONE',  ( 0.000000000000000000, 0.000000000000000000, 1.000000000000000000 ) ) ;
#47001=UNCERTAINTY_MEASURE_WITH_UNIT (LENGTH_MEASURE( 1.000000000000000082E-05 ), #63844, 'distance_accuracy_value', 'NONE');
#47072=MECHANICAL_DESIGN_GEOMETRIC_PRESENTATION_REPRESENTATION('',(#33329),#43689);
#47097=EDGE_CURVE ( 'NONE', #68407, #98268, #101782, .T. ) ;
#47143=VECTOR ( 'NONE', #65669, 1000.000000000000000 ) ;
#47230=ORIENTED_EDGE ( 'NONE', *, *, #10147, .F. ) ;
#47433=CARTESIAN_POINT ( 'NONE',  ( 3.013128138968859560, 20.49583289608097658, -6.321380353784028294 ) ) ;
#47649=CARTESIAN_POINT ( 'NONE',  ( -3.463524195881185097, 15.83536129559750805, -6.085255580401768505 ) ) ;
#47878=DIRECTION ( 'NONE',  ( 1.000000000000000000, 0.000000000000000000, 0.000000000000000000 ) ) ;
#47936=ORIENTED_EDGE ( 'NONE', *, *, #32316, .T. ) ;
#47955=CARTESIAN_POINT ( 'NONE',  ( 3.585913242228626174, 19.64393302524088725, -6.012923278400477578 ) ) ;
#48032=CIRCLE ( 'NONE', #13624, 10.00000000000000178 ) ;
#48289=VECTOR ( 'NONE', #35295, 1000.000000000000000 ) ;
#48745=CARTESIAN_POINT ( 'NONE',  ( 0.5361747445545236301, 13.87998248976673921, -6.984311481106284525 ) ) ;
#48830=AXIS2_PLACEMENT_3D ( 'NONE', #71216, #13501, #45370 ) ;
#49051=DIRECTION ( 'NONE',  ( -0.000000000000000000, -1.000000000000000000, -0.000000000000000000 ) ) ;
#49157=CARTESIAN_POINT ( 'NONE',  ( -3.586716539735087750, 19.64243682284886461, -6.012447941353936898 ) ) ;
#49440=ORIENTED_EDGE ( 'NONE', *, *, #97547, .T. ) ;
#49527=ADVANCED_FACE ( 'NONE', ( #10450 ), #27221, .F. ) ;
#49676=CARTESIAN_POINT ( 'NONE',  ( -4.000000000000000000, 17.85270131633358304, 5.744562646538042827 ) ) ;
#49704=CARTESIAN_POINT ( 'NONE',  ( -3.867509348774311739, 18.90767212923780249, -5.834931863125392582 ) ) ;
#49840=COLOUR_RGB ( '', 0.09019608, 0.27058824, 0.51372549) ;
#50024=CARTESIAN_POINT ( 'NONE',  ( 8.572527594031501786E-16, 2.999999999999992450, 7.000000000000023981 ) ) ;
#50146=ADVANCED_FACE ( 'NONE', ( #68869 ), #95261, .F. ) ;
#50236=CARTESIAN_POINT ( 'NONE',  ( -1.344569080228518650E-17, 21.85270131633358304, -7.000000000000011546 ) ) ;
#50344=CARTESIAN_POINT ( 'NONE',  ( 2.448541588119020673, 14.67925956666102572, -6.561650255352408756 ) ) ;
#50551=LINE ( 'NONE', #42477, #85915 ) ;
#50732=VERTEX_POINT ( 'NONE', #96193 ) ;
#50831=EDGE_CURVE ( 'NONE', #28736, #90523, #33583, .T. ) ;
#50876=CARTESIAN_POINT ( 'NONE',  ( 4.000000000000002665, 17.58193670394227937, -5.744562646538072137 ) ) ;
#51188=FACE_OUTER_BOUND ( 'NONE', #79924, .T. ) ;
#51296=CARTESIAN_POINT ( 'NONE',  ( 3.787807677591960687, 19.16435582558940709, 5.887840124967178568 ) ) ;
#51691=ORIENTED_EDGE ( 'NONE', *, *, #60992, .F. ) ;
#51792=ORIENTED_EDGE ( 'NONE', *, *, #101460, .F. ) ;
#51833=CARTESIAN_POINT ( 'NONE',  ( 2.449319673264149344, 21.02564536029728970, 6.561398256599556333 ) ) ;
#52234=( GEOMETRIC_REPRESENTATION_CONTEXT ( 3 ) GLOBAL_UNCERTAINTY_ASSIGNED_CONTEXT ( ( #47001 ) ) GLOBAL_UNIT_ASSIGNED_CONTEXT ( ( #63844, #16332, #23939 ) ) REPRESENTATION_CONTEXT ( 'NONE', 'WORKASPACE' ) );
#52364=CARTESIAN_POINT ( 'NONE',  ( 4.000000000000000000, 17.85270131633358304, 5.744562646538042827 ) ) ;
#52381=AXIS2_PLACEMENT_3D ( 'NONE', #105610, #89447, #31236 ) ;
#52754=CARTESIAN_POINT ( 'NONE',  ( -4.000000000000000000, 17.85270131633358304, 5.744562646538042827 ) ) ;
#53432=ORIENTED_EDGE ( 'NONE', *, *, #7720, .T. ) ;
#53663=EDGE_CURVE ( 'NONE', #50732, #14213, #56413, .T. ) ;
#53812=CARTESIAN_POINT ( 'NONE',  ( -3.737430656567119147, 19.28391223636466734, 5.919045189202371660 ) ) ;
#54001=EDGE_CURVE ( 'NONE', #11941, #9727, #57788, .T. ) ;
#54286=( NAMED_UNIT ( * ) PLANE_ANGLE_UNIT ( ) SI_UNIT ( $, .RADIAN. ) );
#54479=( LENGTH_UNIT ( ) NAMED_UNIT ( * ) SI_UNIT ( .MILLI., .METRE. ) );
#54670=CARTESIAN_POINT ( 'NONE',  ( -1.313689454042652249, 14.06550833390138777, -6.880078840050021682 ) ) ;
#54963=DIRECTION ( 'NONE',  ( -0.000000000000000000, -1.000000000000000000, -0.000000000000000000 ) ) ;
#55440=DIRECTION ( 'NONE',  ( -0.000000000000000000, -1.000000000000000000, -0.000000000000000000 ) ) ;
#55444=MANIFOLD_SOLID_BREP ( 'Cut-Extrude1', #56674 ) ;
#55645=CARTESIAN_POINT ( 'NONE',  ( -3.013510815085704841, 20.49548354705801501, -6.321220078560170208 ) ) ;
#55725=CARTESIAN_POINT ( 'NONE',  ( -3.787270392904598992, 16.53964648752899791, -5.888179741704394843 ) ) ;
#55791=( GEOMETRIC_REPRESENTATION_CONTEXT ( 3 ) GLOBAL_UNCERTAINTY_ASSIGNED_CONTEXT ( ( #71804 ) ) GLOBAL_UNIT_ASSIGNED_CONTEXT ( ( #55870, #54286, #101927 ) ) REPRESENTATION_CONTEXT ( 'NONE', 'WORKASPACE' ) );
#55870=( LENGTH_UNIT ( ) NAMED_UNIT ( * ) SI_UNIT ( .MILLI., .METRE. ) );
#56413=B_SPLINE_CURVE_WITH_KNOTS ( 'NONE', 3,
 ( #88449, #438, #73837, #32880, #14521, #97051, #33409, #90025, #65755, #47433, #105153, #66278, #47955, #72251, #80862, #81915, #16131, #41473 ),
 .UNSPECIFIED., .F., .F.,
 ( 4, 2, 2, 2, 2, 2, 2, 2, 4 ),
 ( 1.303092495393577094E-20, 0.0008000025724062559277, 0.001600005144812511855, 0.002400007717218767891, 0.003200010289625023711, 0.004000012862031279530, 0.004800015434437535783, 0.005600018006843791168, 0.006400020579250047421 ),
 .UNSPECIFIED. ) ;
#56628=EDGE_LOOP ( 'NONE', ( #77349, #81935, #101857, #3441 ) ) ;
#56674=CLOSED_SHELL ( 'NONE', ( #49527, #18983, #95029, #87857, #75704, #25199, #5412, #29970, #18198, #70987, #50146 ) ) ;
#56764=STYLED_ITEM ( 'NONE', ( #10554 ), #70987 ) ;
#56811=CARTESIAN_POINT ( 'NONE',  ( 3.586311574072714503, 16.06230210627474264, 6.012682668914248296 ) ) ;
#57033=DIRECTION ( 'NONE',  ( 0.000000000000000000, 0.000000000000000000, 1.000000000000000000 ) ) ;
#57753=DIRECTION ( 'NONE',  ( 0.000000000000000000, 0.000000000000000000, -1.000000000000000000 ) ) ;
#57788=B_SPLINE_CURVE_WITH_KNOTS ( 'NONE', 3,
 ( #83519, #42531, #43602, #76493, #75433, #67361, #44686, #19910, #46268, #95348, #29075, #22010, #4213, #37684, #70008, #53812, #30099, #3691, #78096, #86219, #85675, #52754 ),
 .UNSPECIFIED., .F., .F.,
 ( 4, 2, 2, 2, 2, 2, 2, 2, 2, 2, 4 ),
 ( 0.006402890727434164611, 0.006802332259859119809, 0.007201773792284075874, 0.008000656857133985403, 0.008799539921983894064, 0.009598422986833804460, 0.01039730605168371486, 0.01119618911653362352, 0.01159563064895857351, 0.01199507218138352350, 0.01279395524623341308 ),
 .UNSPECIFIED. ) ;
#57822=DIRECTION ( 'NONE',  ( -0.000000000000000000, -1.000000000000000000, -0.000000000000000000 ) ) ;
#57906=CARTESIAN_POINT ( 'NONE',  ( 3.787655175481866809, 16.54064103469220015, -5.887936971919406126 ) ) ;
#57926=DIRECTION ( 'NONE',  ( 0.000000000000000000, -0.000000000000000000, 1.000000000000000000 ) ) ;
#58071=AXIS2_PLACEMENT_3D ( 'NONE', #104942, #31085, #63963 ) ;
#58258=VECTOR ( 'NONE', #14264, 1000.000000000000000 ) ;
#58279=FILL_AREA_STYLE ('',( #99251 ) ) ;
#58373=AXIS2_PLACEMENT_3D ( 'NONE', #80017, #6128, #63867 ) ;
#58459=CARTESIAN_POINT ( 'NONE',  ( 3.461320898197532525, 15.83138828300827150, -6.086543647318008787 ) ) ;
#58557=SHAPE_REPRESENTATION ( '9. Reciprocating Link', ( #10728 ), #52234 ) ;
#58974=ORIENTED_EDGE ( 'NONE', *, *, #17013, .F. ) ;
#59376=FACE_OUTER_BOUND ( 'NONE', #10127, .T. ) ;
#59420=PRODUCT_DEFINITION_FORMATION_WITH_SPECIFIED_SOURCE ( 'ANY', '', #69145, .NOT_KNOWN. ) ;
#59537=CARTESIAN_POINT ( 'NONE',  ( 1.053235267753768190, 13.99157560668549749, -6.921504917287050418 ) ) ;
#59894=CARTESIAN_POINT ( 'NONE',  ( 1.224646799147353454E-15, 2.999999999999993339, 10.00000000000000178 ) ) ;
#60109=DIRECTION ( 'NONE',  ( 1.000000000000000000, 0.000000000000000000, 0.000000000000000000 ) ) ;
#60532=ORIENTED_EDGE ( 'NONE', *, *, #7720, .F. ) ;
#60631=LINE ( 'NONE', #84355, #48289 ) ;
#60846=ORIENTED_EDGE ( 'NONE', *, *, #54001, .F. ) ;
#60857=CARTESIAN_POINT ( 'NONE',  ( 0.000000000000000000, 0.000000000000000000, -10.00000000000000178 ) ) ;
#60884=TOROIDAL_SURFACE ( 'NONE', #48830, 2.000000000000011102, 5.000000000000000000 ) ;
#60992=EDGE_CURVE ( 'NONE', #70408, #98268, #27457, .T. ) ;
#61057=CARTESIAN_POINT ( 'NONE',  ( 0.000000000000000000, -6.505213034913025026E-15, -10.00000000000000178 ) ) ;
#61291=ORIENTED_EDGE ( 'NONE', *, *, #104624, .T. ) ;
#61301=CARTESIAN_POINT ( 'NONE',  ( 0.000000000000000000, 17.85270131633358304, -10.00000000000000178 ) ) ;
#62614=SURFACE_STYLE_USAGE ( .BOTH. , #70700 ) ;
#62799=CARTESIAN_POINT ( 'NONE',  ( -3.177804682974228800, 15.40991233412802330, -6.239222125484262804 ) ) ;
#63317=FILL_AREA_STYLE ('',( #30423 ) ) ;
#63620=AXIS2_PLACEMENT_3D ( 'NONE', #80897, #49051, #63685 ) ;
#63685=DIRECTION ( 'NONE',  ( 0.000000000000000000, 0.000000000000000000, 1.000000000000000000 ) ) ;
#63844=( LENGTH_UNIT ( ) NAMED_UNIT ( * ) SI_UNIT ( .MILLI., .METRE. ) );
#63867=DIRECTION ( 'NONE',  ( 0.000000000000000000, 0.000000000000000000, -1.000000000000000000 ) ) ;
#63883=( GEOMETRIC_REPRESENTATION_CONTEXT ( 3 ) GLOBAL_UNCERTAINTY_ASSIGNED_CONTEXT ( ( #90419 ) ) GLOBAL_UNIT_ASSIGNED_CONTEXT ( ( #3003, #11614, #70409 ) ) REPRESENTATION_CONTEXT ( 'NONE', 'WORKASPACE' ) );
#63963=DIRECTION ( 'NONE',  ( 0.000000000000000000, 0.000000000000000000, 1.000000000000000000 ) ) ;
#64100=ORIENTED_EDGE ( 'NONE', *, *, #342, .F. ) ;
#64907=ORIENTED_EDGE ( 'NONE', *, *, #102859, .T. ) ;
#65351=FACE_OUTER_BOUND ( 'NONE', #76753, .T. ) ;
#65377=ORIENTED_EDGE ( 'NONE', *, *, #100197, .T. ) ;
#65454=CARTESIAN_POINT ( 'NONE',  ( 0.000000000000000000, 200.0000000000000000, 0.000000000000000000 ) ) ;
#65469=AXIS2_PLACEMENT_3D ( 'NONE', #104689, #23265, #29263 ) ;
#65669=DIRECTION ( 'NONE',  ( -0.000000000000000000, -1.000000000000000000, -0.000000000000000000 ) ) ;
#65755=CARTESIAN_POINT ( 'NONE',  ( 2.652922838662404637, 20.85721228183317422, -6.480801738300289827 ) ) ;
#66011=CARTESIAN_POINT ( 'NONE',  ( 1.795343932601242143, 14.26861286782568072, -6.770400604484294149 ) ) ;
#66021=STYLED_ITEM ( 'NONE', ( #24473 ), #94875 ) ;
#66278=CARTESIAN_POINT ( 'NONE',  ( 3.463946997120229021, 19.86939720178062885, -6.085025630164112798 ) ) ;
#66506=CARTESIAN_POINT ( 'NONE',  ( 3.464434906260568603, 15.83682371743314476, 6.084749395801797078 ) ) ;
#66545=CARTESIAN_POINT ( 'NONE',  ( 0.000000000000000000, 2.999999999999992450, 0.000000000000000000 ) ) ;
#66969=CARTESIAN_POINT ( 'NONE',  ( -1.060159942579158798, 21.71876410358088805, -6.924198097909567196 ) ) ;
#67027=CARTESIAN_POINT ( 'NONE',  ( 4.000000000000000000, 17.85270131633358304, -5.744562646538043715 ) ) ;
#67086=CARTESIAN_POINT ( 'NONE',  ( 2.649531230271432225, 14.84514140904274981, -6.482209702755499237 ) ) ;
#67324=AXIS2_PLACEMENT_3D ( 'NONE', #61301, #69392, #11119 ) ;
#67361=CARTESIAN_POINT ( 'NONE',  ( -1.058190070889937440, 21.71930410792606025, 6.924500316192023774 ) ) ;
#67420=ORIENTED_EDGE ( 'NONE', *, *, #100197, .F. ) ;
#67476=CARTESIAN_POINT ( 'NONE',  ( -1.793778237424737965, 14.26790010547893495, 6.770782475500216613 ) ) ;
#67543=CARTESIAN_POINT ( 'NONE',  ( 0.000000000000000000, 2.999999999999993339, 0.000000000000000000 ) ) ;
#67622=CARTESIAN_POINT ( 'NONE',  ( 1.432382586635896571, 14.11565467677096564, -6.853004900836180191 ) ) ;
#67923=DIRECTION ( 'NONE',  ( -0.000000000000000000, -1.000000000000000000, -0.000000000000000000 ) ) ;
#68190=ORIENTED_EDGE ( 'NONE', *, *, #100235, .F. ) ;
#68395=EDGE_CURVE ( 'NONE', #82223, #11941, #50551, .T. ) ;
#68407=VERTEX_POINT ( 'NONE', #10113 ) ;
#68869=FACE_OUTER_BOUND ( 'NONE', #6234, .T. ) ;
#68943=ORIENTED_EDGE ( 'NONE', *, *, #342, .T. ) ;
#69145=PRODUCT ( '9. Reciprocating Link', '9. Reciprocating Link', '', ( #39052 ) ) ;
#69392=DIRECTION ( 'NONE',  ( -0.000000000000000000, -0.000000000000000000, 1.000000000000000000 ) ) ;
#70008=CARTESIAN_POINT ( 'NONE',  ( -3.586915319853207773, 19.64184885895216937, 6.012318516684870495 ) ) ;
#70124=CARTESIAN_POINT ( 'NONE',  ( 8.595526037062774425E-16, 13.85270131633358304, 7.000000000000011546 ) ) ;
#70263=ORIENTED_EDGE ( 'NONE', *, *, #43312, .F. ) ;
#70408=VERTEX_POINT ( 'NONE', #89218 ) ;
#70409=( NAMED_UNIT ( * ) SI_UNIT ( $, .STERADIAN. ) SOLID_ANGLE_UNIT ( ) );
#70700=SURFACE_SIDE_STYLE ('',( #102535 ) ) ;
#70755=CIRCLE ( 'NONE', #100008, 5.000000000000000000 ) ;
#70879=CARTESIAN_POINT ( 'NONE',  ( -2.652798497180052895, 14.84807361897902567, -6.480854662599507598 ) ) ;
#70987=ADVANCED_FACE ( 'NONE', ( #84993 ), #92884, .T. ) ;
#71216=CARTESIAN_POINT ( 'NONE',  ( 0.000000000000000000, 195.0000000000000000, 0.000000000000000000 ) ) ;
#71804=UNCERTAINTY_MEASURE_WITH_UNIT (LENGTH_MEASURE( 1.000000000000000082E-05 ), #55870, 'distance_accuracy_value', 'NONE');
#72251=CARTESIAN_POINT ( 'NONE',  ( 3.787223616631151923, 19.16579769262013500, -5.888204939567934559 ) ) ;
#72331=B_SPLINE_CURVE_WITH_KNOTS ( 'NONE', 3,
 ( #32578, #42223, #143, #41176, #74055, #23969, #663, #90795, #90256, #33629, #83218, #66506, #56811, #15301, #16358, #9313, #98346, #82150 ),
 .UNSPECIFIED., .F., .F.,
 ( 4, 2, 2, 2, 2, 2, 2, 2, 4 ),
 ( 0.01918304055315395856, 0.01998049418066448479, 0.02077794780817501102, 0.02157540143568553379, 0.02237285506319606002, 0.02317030869070658278, 0.02396776231821710901, 0.02476521594572763524, 0.02556266957323816147 ),
 .UNSPECIFIED. ) ;
#72345=EDGE_CURVE ( 'NONE', #14213, #29611, #60631, .T. ) ;
#72388=AXIS2_PLACEMENT_3D ( 'NONE', #43364, #35300, #60109 ) ;
#72828=EDGE_CURVE ( 'NONE', #14645, #70408, #42148, .T. ) ;
#72903=CARTESIAN_POINT ( 'NONE',  ( -4.000000000000000000, 18.12212560230942771, -5.744562646538041051 ) ) ;
#72943=CARTESIAN_POINT ( 'NONE',  ( 8.572527594031486009E-16, 0.000000000000000000, 7.000000000000011546 ) ) ;
#72962=SHAPE_REPRESENTATION_RELATIONSHIP ( 'NONE' , 'NONE' ,  #58557, #94875 ) ;
#73399=ORIENTED_EDGE ( 'NONE', *, *, #19889, .T. ) ;
#73563=LINE ( 'NONE', #16952, #43386 ) ;
#73748=LINE ( 'NONE', #74804, #47143 ) ;
#73837=CARTESIAN_POINT ( 'NONE',  ( 0.5361540264281685619, 21.82547874031371649, -6.984343682103323125 ) ) ;
#74055=CARTESIAN_POINT ( 'NONE',  ( 1.314337315968152620, 14.06570418733889483, 6.879968599000877205 ) ) ;
#74072=CIRCLE ( 'NONE', #65469, 7.000000000000011546 ) ;
#74093=CARTESIAN_POINT ( 'NONE',  ( 3.173243715879570548, 15.40382952331938782, -6.241576743951559259 ) ) ;
#74323=CARTESIAN_POINT ( 'NONE',  ( 0.5336329302387069484, 21.82583525534633395, 6.984546992747041827 ) ) ;
#74562=B_SPLINE_CURVE_WITH_KNOTS ( 'NONE', 3,
 ( #49676, #75002, #10281, #82582, #25996, #83633, #42653, #1096, #34071, #1646, #43193, #34607, #67476, #76077, #27586, #45332, #36741, #70124 ),
 .UNSPECIFIED., .F., .F.,
 ( 4, 2, 2, 2, 2, 2, 2, 2, 4 ),
 ( 0.01279395524623341308, 0.01359259090959848149, 0.01439122657296354989, 0.01518986223632861829, 0.01598849789969368496, 0.01678713356305875509, 0.01758576922642382523, 0.01838440488978889190, 0.01918304055315395856 ),
 .UNSPECIFIED. ) ;
#74583=FACE_OUTER_BOUND ( 'NONE', #27886, .T. ) ;
#74804=CARTESIAN_POINT ( 'NONE',  ( 0.000000000000000000, 0.000000000000000000, -7.000000000000011546 ) ) ;
#74845=CARTESIAN_POINT ( 'NONE',  ( 1.054315034361395842, 21.72038501719248060, 6.925105097140866306 ) ) ;
#74979=PRESENTATION_STYLE_ASSIGNMENT (( #83091 ) ) ;
#75002=CARTESIAN_POINT ( 'NONE',  ( -4.000000000000000888, 17.58270891865066687, 5.744562646538041939 ) ) ;
#75150=CARTESIAN_POINT ( 'NONE',  ( 0.2711492888862935824, 13.85270131633358481, -7.000000000000011546 ) ) ;
#75433=CARTESIAN_POINT ( 'NONE',  ( -0.6682463242654161917, 21.79871736972542351, 6.969258537597399439 ) ) ;
#75702=DIRECTION ( 'NONE',  ( -0.000000000000000000, -1.000000000000000000, -0.000000000000000000 ) ) ;
#75704=ADVANCED_FACE ( 'NONE', ( #74583 ), #2279, .T. ) ;
#75890=CARTESIAN_POINT ( 'NONE',  ( 8.572527594031486009E-16, 195.0000000000000000, 7.000000000000011546 ) ) ;
#76076=DIRECTION ( 'NONE',  ( -0.000000000000000000, -1.000000000000000000, -0.000000000000000000 ) ) ;
#76077=CARTESIAN_POINT ( 'NONE',  ( -1.311584102661731199, 14.06480120835178305, 6.880471120297250387 ) ) ;
#76110=CARTESIAN_POINT ( 'NONE',  ( 2.649924368967711441, 20.85987309459008898, 6.482037363235274796 ) ) ;
#76493=CARTESIAN_POINT ( 'NONE',  ( -0.5366512190794670012, 21.81880124593116221, 6.980675135559732958 ) ) ;
#76753=EDGE_LOOP ( 'NONE', ( #8275, #5544, #49440, #15904, #22114, #26020, #83180, #97468, #64100, #60846 ) ) ;
#77349=ORIENTED_EDGE ( 'NONE', *, *, #19889, .F. ) ;
#77997=LINE ( 'NONE', #86647, #10739 ) ;
#78096=CARTESIAN_POINT ( 'NONE',  ( -3.893533249295163756, 18.77903270381816725, 5.817337832407639020 ) ) ;
#78131=ORIENTED_EDGE ( 'NONE', *, *, #87389, .T. ) ;
#78358=EDGE_CURVE ( 'NONE', #82223, #105779, #74072, .T. ) ;
#79022=DIRECTION ( 'NONE',  ( 0.000000000000000000, 0.000000000000000000, 1.000000000000000000 ) ) ;
#79041=CARTESIAN_POINT ( 'NONE',  ( 0.000000000000000000, 195.0000000000000000, 2.000000000000011102 ) ) ;
#79497=CARTESIAN_POINT ( 'NONE',  ( -4.000000000000000000, 17.58303990196341715, -5.744562646538042827 ) ) ;
#79671=EDGE_LOOP ( 'NONE', ( #43053, #80783, #68943, #53432, #4575, #19969 ) ) ;
#79924=EDGE_LOOP ( 'NONE', ( #33305, #73399, #70263, #51691 ) ) ;
#80017=CARTESIAN_POINT ( 'NONE',  ( 0.000000000000000000, -6.505213034913025026E-15, 0.000000000000000000 ) ) ;
#80546=CARTESIAN_POINT ( 'NONE',  ( -3.013127284365967107, 15.20956086706489963, -6.321382838634907131 ) ) ;
#80783=ORIENTED_EDGE ( 'NONE', *, *, #10147, .T. ) ;
#80862=CARTESIAN_POINT ( 'NONE',  ( 3.866921754057069283, 18.90974295178000730, -5.835322522795916456 ) ) ;
#80897=CARTESIAN_POINT ( 'NONE',  ( 0.000000000000000000, 195.0000000000000000, 0.000000000000000000 ) ) ;
#81258=UNCERTAINTY_MEASURE_WITH_UNIT (LENGTH_MEASURE( 1.000000000000000082E-05 ), #96212, 'distance_accuracy_value', 'NONE');
#81500=CYLINDRICAL_SURFACE ( 'NONE', #101006, 7.000000000000011546 ) ;
#81639=CARTESIAN_POINT ( 'NONE',  ( 3.867124570037480336, 16.79637511870748412, -5.835187682821653787 ) ) ;
#81915=CARTESIAN_POINT ( 'NONE',  ( 3.972670526825609283, 18.38964615182245410, -5.763849554103598116 ) ) ;
#81935=ORIENTED_EDGE ( 'NONE', *, *, #72828, .T. ) ;
#82063=CARTESIAN_POINT ( 'NONE',  ( -3.462314351619998121, 19.87222038490562070, -6.085962419574315163 ) ) ;
#82150=CARTESIAN_POINT ( 'NONE',  ( 4.000000000000000000, 17.85270131633358304, 5.744562646538042827 ) ) ;
#82223=VERTEX_POINT ( 'NONE', #75890 ) ;
#82428=CARTESIAN_POINT ( 'NONE',  ( 4.010857135589731489E-16, 21.85270131633359014, 7.000000000000016875 ) ) ;
#82497=CARTESIAN_POINT ( 'NONE',  ( 0.000000000000000000, 200.0000000000000000, 0.000000000000000000 ) ) ;
#82562=MECHANICAL_DESIGN_GEOMETRIC_PRESENTATION_REPRESENTATION('',(#56764),#63883);
#82582=CARTESIAN_POINT ( 'NONE',  ( -3.866854618780460662, 16.79548022286313724, 5.835366698912954675 ) ) ;
#82609=CARTESIAN_POINT ( 'NONE',  ( -2.652001306203245701, 20.85810219201849947, -6.481200489579615365 ) ) ;
#83091=SURFACE_STYLE_USAGE ( .BOTH. , #17313 ) ;
#83180=ORIENTED_EDGE ( 'NONE', *, *, #87389, .F. ) ;
#83218=CARTESIAN_POINT ( 'NONE',  ( 3.177920610046286676, 15.40997900102463625, 6.239175027651493011 ) ) ;
#83451=CIRCLE ( 'NONE', #26676, 7.000000000000024869 ) ;
#83519=CARTESIAN_POINT ( 'NONE',  ( 4.010857135589731489E-16, 21.85270131633359014, 7.000000000000016875 ) ) ;
#83633=CARTESIAN_POINT ( 'NONE',  ( -3.584918491109374106, 16.05929873264827279, 6.013529126027898464 ) ) ;
#83734=DIRECTION ( 'NONE',  ( 0.000000000000000000, -1.000000000000000000, -0.000000000000000000 ) ) ;
#83779=CARTESIAN_POINT ( 'NONE',  ( -3.222962768498216414E-17, 13.85270131633358304, -7.000000000000011546 ) ) ;
#84006=DIRECTION ( 'NONE',  ( -0.000000000000000000, -1.000000000000000000, -0.000000000000000000 ) ) ;
#84171=CYLINDRICAL_SURFACE ( 'NONE', #100840, 7.000000000000011546 ) ;
#84215=CARTESIAN_POINT ( 'NONE',  ( 3.484468584683845460, 19.88498498222627831, 6.075777484465951339 ) ) ;
#84355=CARTESIAN_POINT ( 'NONE',  ( 4.000000000000000000, 17.85270131633358304, -10.00000000000000178 ) ) ;
#84462=FILL_AREA_STYLE_COLOUR ( '', #49840 ) ;
#84746=CARTESIAN_POINT ( 'NONE',  ( 2.020820481867037888, 21.31435198444414070, 6.705773521646341884 ) ) ;
#84993=FACE_OUTER_BOUND ( 'NONE', #97974, .T. ) ;
#85055=COLOUR_RGB ( '', 0.72549020, 0.75294118, 0.79215686) ;
#85675=CARTESIAN_POINT ( 'NONE',  ( -3.999999999999999112, 18.12277735230508213, 5.744562646538041051 ) ) ;
#85769=EDGE_CURVE ( 'NONE', #29611, #11941, #88868, .T. ) ;
#85915=VECTOR ( 'NONE', #84006, 1000.000000000000000 ) ;
#86219=CARTESIAN_POINT ( 'NONE',  ( -3.972937144959854283, 18.38799044701208985, 5.763666621267263146 ) ) ;
#86647=CARTESIAN_POINT ( 'NONE',  ( -4.000000000000000000, 17.85270131633358304, -10.00000000000000178 ) ) ;
#87389=EDGE_CURVE ( 'NONE', #90523, #36223, #83451, .T. ) ;
#87692=DIRECTION ( 'NONE',  ( -0.000000000000000000, -0.000000000000000000, 1.000000000000000000 ) ) ;
#87857=ADVANCED_FACE ( 'NONE', ( #59376 ), #84171, .T. ) ;
#88183=DIRECTION ( 'NONE',  ( 0.000000000000000000, 1.000000000000000000, 0.000000000000000000 ) ) ;
#88449=CARTESIAN_POINT ( 'NONE',  ( -1.344569080228518650E-17, 21.85270131633358304, -7.000000000000011546 ) ) ;
#88654=CARTESIAN_POINT ( 'NONE',  ( -1.796354877921464421, 14.26916677339775319, -6.770108860242546989 ) ) ;
#88868=B_SPLINE_CURVE_WITH_KNOTS ( 'NONE', 3,
 ( #52364, #92285, #18989, #36240, #51296, #84215, #43227, #76110, #51833, #84746, #26367, #41962, #74845, #74323, #24746, #82428 ),
 .UNSPECIFIED., .F., .F.,
 ( 4, 2, 2, 2, 2, 2, 2, 4 ),
 ( 0.000000000000000000, 0.0008003613409292714437, 0.001600722681858542671, 0.003201445363717083607, 0.004001806704646354400, 0.004802168045575623892, 0.005602529386504895119, 0.006402890727434164611 ),
 .UNSPECIFIED. ) ;
#89100=DIRECTION ( 'NONE',  ( 0.000000000000000000, 0.000000000000000000, -1.000000000000000000 ) ) ;
#89171=SURFACE_STYLE_FILL_AREA ( #63317 ) ;
#89218=CARTESIAN_POINT ( 'NONE',  ( 0.000000000000000000, 2.999999999999993339, -10.00000000000000178 ) ) ;
#89447=DIRECTION ( 'NONE',  ( -0.000000000000000000, -1.000000000000000000, -0.000000000000000000 ) ) ;
#89487=VERTEX_POINT ( 'NONE', #19425 ) ;
#90025=CARTESIAN_POINT ( 'NONE',  ( 2.454882126627601302, 21.02146602321183622, -6.559358972060581827 ) ) ;
#90256=CARTESIAN_POINT ( 'NONE',  ( 2.653887821103243727, 14.84905342050943311, 6.480402264000274748 ) ) ;
#90312=STYLED_ITEM ( 'NONE', ( #74979 ), #55444 ) ;
#90419=UNCERTAINTY_MEASURE_WITH_UNIT (LENGTH_MEASURE( 1.000000000000000082E-05 ), #3003, 'distance_accuracy_value', 'NONE');
#90450=UNCERTAINTY_MEASURE_WITH_UNIT (LENGTH_MEASURE( 1.000000000000000082E-05 ), #54479, 'distance_accuracy_value', 'NONE');
#90523=VERTEX_POINT ( 'NONE', #50024 ) ;
#90565=ORIENTED_EDGE ( 'NONE', *, *, #33609, .F. ) ;
#90795=CARTESIAN_POINT ( 'NONE',  ( 2.455632601332660148, 14.68453990184912428, 6.559068799100592706 ) ) ;
#91140=DIRECTION ( 'NONE',  ( 0.000000000000000000, 1.000000000000000000, 0.000000000000000000 ) ) ;
#91206=SURFACE_STYLE_FILL_AREA ( #58279 ) ;
#91773=CARTESIAN_POINT ( 'NONE',  ( -0.2701328141633552726, 21.85270131633358304, -7.000000000000010658 ) ) ;
#91879=ORIENTED_EDGE ( 'NONE', *, *, #53663, .F. ) ;
#91976=DIRECTION ( 'NONE',  ( 1.224646799147353207E-16, 0.000000000000000000, -1.000000000000000000 ) ) ;
#92010=FILL_AREA_STYLE ('',( #84462 ) ) ;
#92285=CARTESIAN_POINT ( 'NONE',  ( 4.000000000000001776, 18.12398157863135850, 5.744562646538044604 ) ) ;
#92884=TOROIDAL_SURFACE ( 'NONE', #13658, 2.000000000000011102, 5.000000000000000000 ) ;
#93265=DIRECTION ( 'NONE',  ( 0.000000000000000000, 0.000000000000000000, -1.000000000000000000 ) ) ;
#94650=CARTESIAN_POINT ( 'NONE',  ( -3.972507935376086596, 17.31478156112088485, -5.763960839875241327 ) ) ;
#94875=ADVANCED_BREP_SHAPE_REPRESENTATION ( '', ( #55444, #10728 ), #52234 ) ;
#95029=ADVANCED_FACE ( 'NONE', ( #51188 ), #10206, .T. ) ;
#95261=CYLINDRICAL_SURFACE ( 'NONE', #67324, 4.000000000000000000 ) ;
#95348=CARTESIAN_POINT ( 'NONE',  ( -2.455519666312785620, 21.02091283430367241, 6.559096923523866529 ) ) ;
#95500=( NAMED_UNIT ( * ) PLANE_ANGLE_UNIT ( ) SI_UNIT ( $, .RADIAN. ) );
#95687=CARTESIAN_POINT ( 'NONE',  ( -4.000000000000000000, 17.85270131633358659, -5.744562646538044604 ) ) ;
#96193=CARTESIAN_POINT ( 'NONE',  ( -1.344569080228518650E-17, 21.85270131633358304, -7.000000000000011546 ) ) ;
#96212=( LENGTH_UNIT ( ) NAMED_UNIT ( * ) SI_UNIT ( .MILLI., .METRE. ) );
#96268=CARTESIAN_POINT ( 'NONE',  ( 0.000000000000000000, 195.0000000000000000, -7.000000000000011546 ) ) ;
#96272=CIRCLE ( 'NONE', #58373, 10.00000000000000178 ) ;
#96673=CARTESIAN_POINT ( 'NONE',  ( -3.175336665761835597, 20.29878287605892595, -6.240496478724519847 ) ) ;
#97023=ORIENTED_EDGE ( 'NONE', *, *, #50831, .T. ) ;
#97051=CARTESIAN_POINT ( 'NONE',  ( 1.796381498081899508, 21.43623042924785693, -6.770105592763798086 ) ) ;
#97250=SURFACE_SIDE_STYLE ('',( #89171 ) ) ;
#97468=ORIENTED_EDGE ( 'NONE', *, *, #50831, .F. ) ;
#97547=EDGE_CURVE ( 'NONE', #105779, #50732, #73748, .T. ) ;
#97974=EDGE_LOOP ( 'NONE', ( #99797, #15760, #16133, #99924 ) ) ;
#98130=CARTESIAN_POINT ( 'NONE',  ( 0.000000000000000000, -6.505213034913025026E-15, 0.000000000000000000 ) ) ;
#98268=VERTEX_POINT ( 'NONE', #61057 ) ;
#98346=CARTESIAN_POINT ( 'NONE',  ( 4.000000000000001776, 17.58240661545486105, 5.744562646538042827 ) ) ;
#98775=CARTESIAN_POINT ( 'NONE',  ( -3.973065139046256800, 18.38687860884221337, -5.763576303916519983 ) ) ;
#98889=CARTESIAN_POINT ( 'NONE',  ( 1.306730854166997080, 14.06983854460715300, -6.878153045988232073 ) ) ;
#99180=DIRECTION ( 'NONE',  ( 0.000000000000000000, 0.000000000000000000, -1.000000000000000000 ) ) ;
#99251=FILL_AREA_STYLE_COLOUR ( '', #17956 ) ;
#99422=DIRECTION ( 'NONE',  ( -0.000000000000000000, -1.000000000000000000, -0.000000000000000000 ) ) ;
#99442=DIRECTION ( 'NONE',  ( 0.000000000000000000, 1.000000000000000000, 0.000000000000000000 ) ) ;
#99797=ORIENTED_EDGE ( 'NONE', *, *, #104624, .F. ) ;
#99892=DIRECTION ( 'NONE',  ( 0.000000000000000000, 0.000000000000000000, -1.000000000000000000 ) ) ;
#99924=ORIENTED_EDGE ( 'NONE', *, *, #102859, .F. ) ;
#100008=AXIS2_PLACEMENT_3D ( 'NONE', #79041, #13758, #46668 ) ;
#100197=EDGE_CURVE ( 'NONE', #36223, #90523, #32081, .T. ) ;
#100235=EDGE_CURVE ( 'NONE', #14213, #21895, #14518, .T. ) ;
#100380=CARTESIAN_POINT ( 'NONE',  ( -1.315122544340494137, 21.63948755414514125, -6.879847735748377602 ) ) ;
#100395=ORIENTED_EDGE ( 'NONE', *, *, #54001, .T. ) ;
#100439=MECHANICAL_DESIGN_GEOMETRIC_PRESENTATION_REPRESENTATION('',(#66021),#19581);
#100461=DIRECTION ( 'NONE',  ( 0.000000000000000000, 0.000000000000000000, -1.000000000000000000 ) ) ;
#100840=AXIS2_PLACEMENT_3D ( 'NONE', #104055, #54963, #29684 ) ;
#101006=AXIS2_PLACEMENT_3D ( 'NONE', #15731, #40538, #89100 ) ;
#101460=EDGE_CURVE ( 'NONE', #17102, #31486, #42598, .T. ) ;
#101782=CIRCLE ( 'NONE', #46653, 10.00000000000000178 ) ;
#101857=ORIENTED_EDGE ( 'NONE', *, *, #60992, .T. ) ;
#101927=( NAMED_UNIT ( * ) SI_UNIT ( $, .STERADIAN. ) SOLID_ANGLE_UNIT ( ) );
#101952=CARTESIAN_POINT ( 'NONE',  ( 5.510910596163103361E-16, 200.0000000000000000, -2.000000000000011102 ) ) ;
#102535=SURFACE_STYLE_FILL_AREA ( #4905 ) ;
#102859=EDGE_CURVE ( 'NONE', #31486, #17102, #24263, .T. ) ;
#103251=CARTESIAN_POINT ( 'NONE',  ( -2.024833989188797645, 14.39326063602704942, -6.704610268883726576 ) ) ;
#103439=FACE_OUTER_BOUND ( 'NONE', #22515, .T. ) ;
#103718=DIRECTION ( 'NONE',  ( 0.000000000000000000, 0.000000000000000000, -1.000000000000000000 ) ) ;
#103773=CARTESIAN_POINT ( 'NONE',  ( -3.866873951915034802, 16.79560018603664417, -5.835353434046841592 ) ) ;
#103822=CARTESIAN_POINT ( 'NONE',  ( 0.000000000000000000, 195.0000000000000000, 0.000000000000000000 ) ) ;
#104055=CARTESIAN_POINT ( 'NONE',  ( 0.000000000000000000, 0.000000000000000000, 0.000000000000000000 ) ) ;
#104109=FILL_AREA_STYLE_COLOUR ( '', #85055 ) ;
#104624=EDGE_CURVE ( 'NONE', #105779, #31486, #19357, .T. ) ;
#104689=CARTESIAN_POINT ( 'NONE',  ( 0.000000000000000000, 195.0000000000000000, 0.000000000000000000 ) ) ;
#104942=CARTESIAN_POINT ( 'NONE',  ( 0.000000000000000000, 200.0000000000000000, 0.000000000000000000 ) ) ;
#105097=CYLINDRICAL_SURFACE ( 'NONE', #52381, 10.00000000000000178 ) ;
#105153=CARTESIAN_POINT ( 'NONE',  ( 3.177522834362841664, 20.29592454198039775, -6.239376119109595997 ) ) ;
#105300=ORIENTED_EDGE ( 'NONE', *, *, #12003, .F. ) ;
#105610=CARTESIAN_POINT ( 'NONE',  ( 0.000000000000000000, 0.000000000000000000, 0.000000000000000000 ) ) ;
#105779=VERTEX_POINT ( 'NONE', #96268 ) ;
#105813=CARTESIAN_POINT ( 'NONE',  ( -3.788334298886703255, 19.16274404829667688, -5.887494290764028193 ) ) ;
ENDSEC;
END-ISO-10303-21;
